ISO-10303-21;
HEADER;
/* Generated by software containing ST-Developer
 * from STEP Tools, Inc. (www.steptools.com) 
 */

FILE_DESCRIPTION(
/* description */ ('Overhung pulley bearing cartridge'),
/* implementation_level */ '2;1');

FILE_NAME(
/* name */ 'Cap Screw - M6x25.step',
/* time_stamp */ '2026-10-28T03:22:33-07:00',
/* author */ (''),
/* organization */ (''),
/* preprocessor_version */ 'ST-DEVELOPER v20.2',
/* originating_system */ 'Autodesk Translation Framework v15.17.0.0',
/* authorisation */ '');

FILE_SCHEMA (('AUTOMOTIVE_DESIGN { 1 0 10303 214 3 1 1 }'));
ENDSEC;

DATA;
#10=MECHANICAL_DESIGN_GEOMETRIC_PRESENTATION_REPRESENTATION('',(#304),#10963);
#11=ORIENTED_CLOSED_SHELL('',*,#5672,.F.);
#13=BREP_WITH_VOIDS('Body1',#5671,(#11));
#227=CONICAL_SURFACE('',#6248,0.475,0.785398163397449);
#228=CONICAL_SURFACE('',#6252,0.485,0.785398163397448);
#229=CONICAL_SURFACE('',#6256,0.31,0.463647609000806);
#230=CONICAL_SURFACE('',#6260,0.27,0.785398163397448);
#252=SHAPE_REPRESENTATION_RELATIONSHIP('SRR','None',#11073,#274);
#274=ADVANCED_BREP_SHAPE_REPRESENTATION('',(#13),#10953);
#304=STYLED_ITEM('',(#11260),#13);
#405=FACE_BOUND('',#1120,.T.);
#508=PLANE('',#6246);
#509=PLANE('',#6254);
#510=PLANE('',#6262);
#511=PLANE('',#6263);
#512=PLANE('',#6264);
#513=PLANE('',#6265);
#514=PLANE('',#6266);
#515=PLANE('',#6267);
#516=PLANE('',#6268);
#517=PLANE('',#6269);
#518=PLANE('',#6270);
#722=FACE_OUTER_BOUND('',#1115,.T.);
#723=FACE_OUTER_BOUND('',#1116,.T.);
#724=FACE_OUTER_BOUND('',#1117,.T.);
#725=FACE_OUTER_BOUND('',#1118,.T.);
#726=FACE_OUTER_BOUND('',#1119,.T.);
#727=FACE_OUTER_BOUND('',#1121,.T.);
#728=FACE_OUTER_BOUND('',#1122,.T.);
#729=FACE_OUTER_BOUND('',#1123,.T.);
#730=FACE_OUTER_BOUND('',#1124,.T.);
#731=FACE_OUTER_BOUND('',#1125,.T.);
#732=FACE_OUTER_BOUND('',#1126,.T.);
#733=FACE_OUTER_BOUND('',#1127,.T.);
#734=FACE_OUTER_BOUND('',#1128,.T.);
#735=FACE_OUTER_BOUND('',#1129,.T.);
#736=FACE_OUTER_BOUND('',#1130,.T.);
#737=FACE_OUTER_BOUND('',#1131,.T.);
#738=FACE_OUTER_BOUND('',#1132,.T.);
#1115=EDGE_LOOP('',(#4247));
#1116=EDGE_LOOP('',(#4248,#4249,#4250,#4251));
#1117=EDGE_LOOP('',(#4252,#4253,#4254,#4255));
#1118=EDGE_LOOP('',(#4256,#4257,#4258,#4259));
#1119=EDGE_LOOP('',(#4260));
#1120=EDGE_LOOP('',(#4261));
#1121=EDGE_LOOP('',(#4262,#4263,#4264,#4265));
#1122=EDGE_LOOP('',(#4266,#4267,#4268,#4269));
#1123=EDGE_LOOP('',(#4270,#4271,#4272,#4273));
#1124=EDGE_LOOP('',(#4274));
#1125=EDGE_LOOP('',(#4275,#4276,#4277,#4278));
#1126=EDGE_LOOP('',(#4279,#4280,#4281,#4282));
#1127=EDGE_LOOP('',(#4283,#4284,#4285,#4286));
#1128=EDGE_LOOP('',(#4287,#4288,#4289,#4290));
#1129=EDGE_LOOP('',(#4291,#4292,#4293,#4294));
#1130=EDGE_LOOP('',(#4295,#4296,#4297,#4298));
#1131=EDGE_LOOP('',(#4299,#4300,#4301,#4302,#4303,#4304));
#1132=EDGE_LOOP('',(#4305,#4306,#4307,#4308,#4309,#4310));
#1453=LINE('',#9570,#1795);
#1454=LINE('',#9574,#1796);
#1455=LINE('',#9578,#1797);
#1456=LINE('',#9585,#1798);
#1457=LINE('',#9589,#1799);
#1458=LINE('',#9593,#1800);
#1459=LINE('',#9598,#1801);
#1460=LINE('',#9600,#1802);
#1461=LINE('',#9602,#1803);
#1462=LINE('',#9603,#1804);
#1463=LINE('',#9606,#1805);
#1464=LINE('',#9608,#1806);
#1465=LINE('',#9609,#1807);
#1466=LINE('',#9612,#1808);
#1467=LINE('',#9614,#1809);
#1468=LINE('',#9615,#1810);
#1469=LINE('',#9618,#1811);
#1470=LINE('',#9620,#1812);
#1471=LINE('',#9621,#1813);
#1472=LINE('',#9624,#1814);
#1473=LINE('',#9626,#1815);
#1474=LINE('',#9627,#1816);
#1475=LINE('',#9629,#1817);
#1476=LINE('',#9630,#1818);
#1795=VECTOR('',#7463,0.475);
#1796=VECTOR('',#7468,0.5);
#1797=VECTOR('',#7473,0.485);
#1798=VECTOR('',#7482,0.31);
#1799=VECTOR('',#7487,0.3);
#1800=VECTOR('',#7492,0.27);
#1801=VECTOR('',#7497,1.);
#1802=VECTOR('',#7498,1.);
#1803=VECTOR('',#7499,1.);
#1804=VECTOR('',#7500,1.);
#1805=VECTOR('',#7503,1.);
#1806=VECTOR('',#7504,1.);
#1807=VECTOR('',#7505,1.);
#1808=VECTOR('',#7508,1.);
#1809=VECTOR('',#7509,1.);
#1810=VECTOR('',#7510,1.);
#1811=VECTOR('',#7513,1.);
#1812=VECTOR('',#7514,1.);
#1813=VECTOR('',#7515,1.);
#1814=VECTOR('',#7518,1.);
#1815=VECTOR('',#7519,1.);
#1816=VECTOR('',#7520,1.);
#1817=VECTOR('',#7523,1.);
#1818=VECTOR('',#7524,1.);
#2166=CIRCLE('',#6247,0.45);
#2167=CIRCLE('',#6249,0.5);
#2168=CIRCLE('',#6251,0.5);
#2169=CIRCLE('',#6253,0.47);
#2170=CIRCLE('',#6255,0.32);
#2171=CIRCLE('',#6257,0.2942);
#2172=CIRCLE('',#6259,0.2942);
#2173=CIRCLE('',#6261,0.24);
#2589=VERTEX_POINT('',#9565);
#2590=VERTEX_POINT('',#9568);
#2591=VERTEX_POINT('',#9572);
#2592=VERTEX_POINT('',#9576);
#2593=VERTEX_POINT('',#9580);
#2594=VERTEX_POINT('',#9583);
#2595=VERTEX_POINT('',#9587);
#2596=VERTEX_POINT('',#9591);
#2597=VERTEX_POINT('',#9596);
#2598=VERTEX_POINT('',#9597);
#2599=VERTEX_POINT('',#9599);
#2600=VERTEX_POINT('',#9601);
#2601=VERTEX_POINT('',#9605);
#2602=VERTEX_POINT('',#9607);
#2603=VERTEX_POINT('',#9611);
#2604=VERTEX_POINT('',#9613);
#2605=VERTEX_POINT('',#9617);
#2606=VERTEX_POINT('',#9619);
#2607=VERTEX_POINT('',#9623);
#2608=VERTEX_POINT('',#9625);
#3193=EDGE_CURVE('',#2589,#2589,#2166,.T.);
#3194=EDGE_CURVE('',#2590,#2590,#2167,.T.);
#3195=EDGE_CURVE('',#2590,#2589,#1453,.T.);
#3196=EDGE_CURVE('',#2591,#2591,#2168,.T.);
#3197=EDGE_CURVE('',#2591,#2590,#1454,.T.);
#3198=EDGE_CURVE('',#2592,#2592,#2169,.T.);
#3199=EDGE_CURVE('',#2592,#2591,#1455,.T.);
#3200=EDGE_CURVE('',#2593,#2593,#2170,.T.);
#3201=EDGE_CURVE('',#2594,#2594,#2171,.F.);
#3202=EDGE_CURVE('',#2594,#2593,#1456,.T.);
#3203=EDGE_CURVE('',#2595,#2595,#2172,.F.);
#3204=EDGE_CURVE('',#2595,#2594,#1457,.T.);
#3205=EDGE_CURVE('',#2596,#2596,#2173,.T.);
#3206=EDGE_CURVE('',#2596,#2595,#1458,.T.);
#3207=EDGE_CURVE('',#2597,#2598,#1459,.T.);
#3208=EDGE_CURVE('',#2598,#2599,#1460,.T.);
#3209=EDGE_CURVE('',#2599,#2600,#1461,.T.);
#3210=EDGE_CURVE('',#2597,#2600,#1462,.T.);
#3211=EDGE_CURVE('',#2598,#2601,#1463,.T.);
#3212=EDGE_CURVE('',#2601,#2602,#1464,.T.);
#3213=EDGE_CURVE('',#2602,#2599,#1465,.T.);
#3214=EDGE_CURVE('',#2601,#2603,#1466,.T.);
#3215=EDGE_CURVE('',#2603,#2604,#1467,.T.);
#3216=EDGE_CURVE('',#2604,#2602,#1468,.T.);
#3217=EDGE_CURVE('',#2603,#2605,#1469,.T.);
#3218=EDGE_CURVE('',#2605,#2606,#1470,.T.);
#3219=EDGE_CURVE('',#2606,#2604,#1471,.T.);
#3220=EDGE_CURVE('',#2605,#2607,#1472,.T.);
#3221=EDGE_CURVE('',#2607,#2608,#1473,.T.);
#3222=EDGE_CURVE('',#2608,#2606,#1474,.T.);
#3223=EDGE_CURVE('',#2607,#2597,#1475,.T.);
#3224=EDGE_CURVE('',#2600,#2608,#1476,.T.);
#4247=ORIENTED_EDGE('',*,*,#3193,.F.);
#4248=ORIENTED_EDGE('',*,*,#3194,.F.);
#4249=ORIENTED_EDGE('',*,*,#3195,.T.);
#4250=ORIENTED_EDGE('',*,*,#3193,.T.);
#4251=ORIENTED_EDGE('',*,*,#3195,.F.);
#4252=ORIENTED_EDGE('',*,*,#3196,.F.);
#4253=ORIENTED_EDGE('',*,*,#3197,.T.);
#4254=ORIENTED_EDGE('',*,*,#3194,.T.);
#4255=ORIENTED_EDGE('',*,*,#3197,.F.);
#4256=ORIENTED_EDGE('',*,*,#3198,.F.);
#4257=ORIENTED_EDGE('',*,*,#3199,.T.);
#4258=ORIENTED_EDGE('',*,*,#3196,.T.);
#4259=ORIENTED_EDGE('',*,*,#3199,.F.);
#4260=ORIENTED_EDGE('',*,*,#3198,.T.);
#4261=ORIENTED_EDGE('',*,*,#3200,.F.);
#4262=ORIENTED_EDGE('',*,*,#3201,.F.);
#4263=ORIENTED_EDGE('',*,*,#3202,.T.);
#4264=ORIENTED_EDGE('',*,*,#3200,.T.);
#4265=ORIENTED_EDGE('',*,*,#3202,.F.);
#4266=ORIENTED_EDGE('',*,*,#3203,.F.);
#4267=ORIENTED_EDGE('',*,*,#3204,.T.);
#4268=ORIENTED_EDGE('',*,*,#3201,.T.);
#4269=ORIENTED_EDGE('',*,*,#3204,.F.);
#4270=ORIENTED_EDGE('',*,*,#3205,.F.);
#4271=ORIENTED_EDGE('',*,*,#3206,.T.);
#4272=ORIENTED_EDGE('',*,*,#3203,.T.);
#4273=ORIENTED_EDGE('',*,*,#3206,.F.);
#4274=ORIENTED_EDGE('',*,*,#3205,.T.);
#4275=ORIENTED_EDGE('',*,*,#3207,.T.);
#4276=ORIENTED_EDGE('',*,*,#3208,.T.);
#4277=ORIENTED_EDGE('',*,*,#3209,.T.);
#4278=ORIENTED_EDGE('',*,*,#3210,.F.);
#4279=ORIENTED_EDGE('',*,*,#3211,.T.);
#4280=ORIENTED_EDGE('',*,*,#3212,.T.);
#4281=ORIENTED_EDGE('',*,*,#3213,.T.);
#4282=ORIENTED_EDGE('',*,*,#3208,.F.);
#4283=ORIENTED_EDGE('',*,*,#3214,.T.);
#4284=ORIENTED_EDGE('',*,*,#3215,.T.);
#4285=ORIENTED_EDGE('',*,*,#3216,.T.);
#4286=ORIENTED_EDGE('',*,*,#3212,.F.);
#4287=ORIENTED_EDGE('',*,*,#3217,.T.);
#4288=ORIENTED_EDGE('',*,*,#3218,.T.);
#4289=ORIENTED_EDGE('',*,*,#3219,.T.);
#4290=ORIENTED_EDGE('',*,*,#3215,.F.);
#4291=ORIENTED_EDGE('',*,*,#3220,.T.);
#4292=ORIENTED_EDGE('',*,*,#3221,.T.);
#4293=ORIENTED_EDGE('',*,*,#3222,.T.);
#4294=ORIENTED_EDGE('',*,*,#3218,.F.);
#4295=ORIENTED_EDGE('',*,*,#3223,.T.);
#4296=ORIENTED_EDGE('',*,*,#3210,.T.);
#4297=ORIENTED_EDGE('',*,*,#3224,.T.);
#4298=ORIENTED_EDGE('',*,*,#3221,.F.);
#4299=ORIENTED_EDGE('',*,*,#3223,.F.);
#4300=ORIENTED_EDGE('',*,*,#3220,.F.);
#4301=ORIENTED_EDGE('',*,*,#3217,.F.);
#4302=ORIENTED_EDGE('',*,*,#3214,.F.);
#4303=ORIENTED_EDGE('',*,*,#3211,.F.);
#4304=ORIENTED_EDGE('',*,*,#3207,.F.);
#4305=ORIENTED_EDGE('',*,*,#3224,.F.);
#4306=ORIENTED_EDGE('',*,*,#3209,.F.);
#4307=ORIENTED_EDGE('',*,*,#3213,.F.);
#4308=ORIENTED_EDGE('',*,*,#3216,.F.);
#4309=ORIENTED_EDGE('',*,*,#3219,.F.);
#4310=ORIENTED_EDGE('',*,*,#3222,.F.);
#5216=CYLINDRICAL_SURFACE('',#6250,0.5);
#5217=CYLINDRICAL_SURFACE('',#6258,0.2942);
#5466=ADVANCED_FACE('',(#722),#508,.T.);
#5467=ADVANCED_FACE('',(#723),#227,.T.);
#5468=ADVANCED_FACE('',(#724),#5216,.T.);
#5469=ADVANCED_FACE('',(#725),#228,.T.);
#5470=ADVANCED_FACE('',(#726,#405),#509,.T.);
#5471=ADVANCED_FACE('',(#727),#229,.T.);
#5472=ADVANCED_FACE('',(#728),#5217,.T.);
#5473=ADVANCED_FACE('',(#729),#230,.T.);
#5474=ADVANCED_FACE('',(#730),#510,.T.);
#5475=ADVANCED_FACE('',(#731),#511,.F.);
#5476=ADVANCED_FACE('',(#732),#512,.F.);
#5477=ADVANCED_FACE('',(#733),#513,.F.);
#5478=ADVANCED_FACE('',(#734),#514,.F.);
#5479=ADVANCED_FACE('',(#735),#515,.F.);
#5480=ADVANCED_FACE('',(#736),#516,.F.);
#5481=ADVANCED_FACE('',(#737),#517,.F.);
#5482=ADVANCED_FACE('',(#738),#518,.F.);
#5671=CLOSED_SHELL('',(#5466,#5467,#5468,#5469,#5470,#5471,#5472,#5473,
#5474));
#5672=CLOSED_SHELL('',(#5475,#5476,#5477,#5478,#5479,#5480,#5481,#5482));
#6245=AXIS2_PLACEMENT_3D('',#9563,#7453,#7454);
#6246=AXIS2_PLACEMENT_3D('',#9564,#7455,#7456);
#6247=AXIS2_PLACEMENT_3D('',#9566,#7457,#7458);
#6248=AXIS2_PLACEMENT_3D('',#9567,#7459,#7460);
#6249=AXIS2_PLACEMENT_3D('',#9569,#7461,#7462);
#6250=AXIS2_PLACEMENT_3D('',#9571,#7464,#7465);
#6251=AXIS2_PLACEMENT_3D('',#9573,#7466,#7467);
#6252=AXIS2_PLACEMENT_3D('',#9575,#7469,#7470);
#6253=AXIS2_PLACEMENT_3D('',#9577,#7471,#7472);
#6254=AXIS2_PLACEMENT_3D('',#9579,#7474,#7475);
#6255=AXIS2_PLACEMENT_3D('',#9581,#7476,#7477);
#6256=AXIS2_PLACEMENT_3D('',#9582,#7478,#7479);
#6257=AXIS2_PLACEMENT_3D('',#9584,#7480,#7481);
#6258=AXIS2_PLACEMENT_3D('',#9586,#7483,#7484);
#6259=AXIS2_PLACEMENT_3D('',#9588,#7485,#7486);
#6260=AXIS2_PLACEMENT_3D('',#9590,#7488,#7489);
#6261=AXIS2_PLACEMENT_3D('',#9592,#7490,#7491);
#6262=AXIS2_PLACEMENT_3D('',#9594,#7493,#7494);
#6263=AXIS2_PLACEMENT_3D('',#9595,#7495,#7496);
#6264=AXIS2_PLACEMENT_3D('',#9604,#7501,#7502);
#6265=AXIS2_PLACEMENT_3D('',#9610,#7506,#7507);
#6266=AXIS2_PLACEMENT_3D('',#9616,#7511,#7512);
#6267=AXIS2_PLACEMENT_3D('',#9622,#7516,#7517);
#6268=AXIS2_PLACEMENT_3D('',#9628,#7521,#7522);
#6269=AXIS2_PLACEMENT_3D('',#9631,#7525,#7526);
#6270=AXIS2_PLACEMENT_3D('',#9632,#7527,#7528);
#7453=DIRECTION('axis',(0.,0.,1.));
#7454=DIRECTION('refdir',(1.,0.,0.));
#7455=DIRECTION('center_axis',(0.,1.,0.));
#7456=DIRECTION('ref_axis',(0.,0.,1.));
#7457=DIRECTION('center_axis',(0.,-1.,0.));
#7458=DIRECTION('ref_axis',(1.,0.,0.));
#7459=DIRECTION('center_axis',(0.,-1.,0.));
#7460=DIRECTION('ref_axis',(1.,0.,0.));
#7461=DIRECTION('center_axis',(0.,-1.,0.));
#7462=DIRECTION('ref_axis',(1.,0.,0.));
#7463=DIRECTION('',(0.707106781186548,0.707106781186547,8.65956056235494E-17));
#7464=DIRECTION('center_axis',(0.,-1.,0.));
#7465=DIRECTION('ref_axis',(1.,0.,0.));
#7466=DIRECTION('center_axis',(0.,-1.,0.));
#7467=DIRECTION('ref_axis',(1.,0.,0.));
#7468=DIRECTION('',(0.,1.,0.));
#7469=DIRECTION('center_axis',(0.,1.,0.));
#7470=DIRECTION('ref_axis',(1.,0.,0.));
#7471=DIRECTION('center_axis',(0.,-1.,0.));
#7472=DIRECTION('ref_axis',(1.,0.,0.));
#7473=DIRECTION('',(-0.707106781186547,0.707106781186548,-8.65956056235493E-17));
#7474=DIRECTION('center_axis',(0.,-1.,0.));
#7475=DIRECTION('ref_axis',(0.,0.,-1.));
#7476=DIRECTION('center_axis',(0.,-1.,0.));
#7477=DIRECTION('ref_axis',(1.,0.,0.));
#7478=DIRECTION('center_axis',(0.,1.,0.));
#7479=DIRECTION('ref_axis',(1.,0.,0.));
#7480=DIRECTION('center_axis',(0.,1.,0.));
#7481=DIRECTION('ref_axis',(1.,0.,0.));
#7482=DIRECTION('',(-0.447213595499958,0.894427190999916,-5.47678698264203E-17));
#7483=DIRECTION('center_axis',(0.,-1.,0.));
#7484=DIRECTION('ref_axis',(1.,0.,0.));
#7485=DIRECTION('center_axis',(0.,1.,0.));
#7486=DIRECTION('ref_axis',(1.,0.,0.));
#7487=DIRECTION('',(0.,1.,0.));
#7488=DIRECTION('center_axis',(0.,1.,0.));
#7489=DIRECTION('ref_axis',(1.,0.,0.));
#7490=DIRECTION('center_axis',(0.,-1.,0.));
#7491=DIRECTION('ref_axis',(1.,0.,0.));
#7492=DIRECTION('',(-0.707106781186547,0.707106781186548,-8.65956056235493E-17));
#7493=DIRECTION('center_axis',(0.,-1.,0.));
#7494=DIRECTION('ref_axis',(0.,0.,-1.));
#7495=DIRECTION('center_axis',(0.866025403784439,0.,-0.5));
#7496=DIRECTION('ref_axis',(0.5,0.,0.866025403784439));
#7497=DIRECTION('',(-0.5,0.,-0.866025403784439));
#7498=DIRECTION('',(0.,-1.,0.));
#7499=DIRECTION('',(0.5,0.,0.866025403784439));
#7500=DIRECTION('',(0.,-1.,0.));
#7501=DIRECTION('center_axis',(1.92296268638356E-16,0.,-1.));
#7502=DIRECTION('ref_axis',(1.,0.,1.92296268638356E-16));
#7503=DIRECTION('',(-1.,0.,-1.92296268638356E-16));
#7504=DIRECTION('',(0.,-1.,0.));
#7505=DIRECTION('',(1.,0.,1.92296268638356E-16));
#7506=DIRECTION('center_axis',(-0.866025403784439,0.,-0.5));
#7507=DIRECTION('ref_axis',(0.5,0.,-0.866025403784439));
#7508=DIRECTION('',(-0.5,0.,0.866025403784438));
#7509=DIRECTION('',(0.,-1.,0.));
#7510=DIRECTION('',(0.5,0.,-0.866025403784438));
#7511=DIRECTION('center_axis',(-0.866025403784439,0.,0.5));
#7512=DIRECTION('ref_axis',(-0.5,0.,-0.866025403784439));
#7513=DIRECTION('',(0.5,0.,0.866025403784439));
#7514=DIRECTION('',(0.,-1.,0.));
#7515=DIRECTION('',(-0.5,0.,-0.866025403784439));
#7516=DIRECTION('center_axis',(-1.92296268638356E-16,0.,1.));
#7517=DIRECTION('ref_axis',(-1.,0.,-1.92296268638356E-16));
#7518=DIRECTION('',(1.,0.,1.92296268638356E-16));
#7519=DIRECTION('',(0.,-1.,0.));
#7520=DIRECTION('',(-1.,0.,-1.92296268638356E-16));
#7521=DIRECTION('center_axis',(0.866025403784439,0.,0.5));
#7522=DIRECTION('ref_axis',(-0.5,0.,0.866025403784439));
#7523=DIRECTION('',(0.5,0.,-0.866025403784439));
#7524=DIRECTION('',(-0.5,0.,0.866025403784439));
#7525=DIRECTION('center_axis',(0.,1.,0.));
#7526=DIRECTION('ref_axis',(1.,0.,0.));
#7527=DIRECTION('center_axis',(0.,-1.,0.));
#7528=DIRECTION('ref_axis',(0.,0.,-1.));
#9563=CARTESIAN_POINT('',(0.,0.,0.));
#9564=CARTESIAN_POINT('Origin',(0.45,0.6,0.));
#9565=CARTESIAN_POINT('',(-0.45,0.6,-5.51091059616309E-17));
#9566=CARTESIAN_POINT('Origin',(0.,0.6,0.));
#9567=CARTESIAN_POINT('Origin',(0.,0.575,0.));
#9568=CARTESIAN_POINT('',(-0.5,0.55,-6.12323399573677E-17));
#9569=CARTESIAN_POINT('Origin',(0.,0.55,0.));
#9570=CARTESIAN_POINT('',(-0.475,0.575,-5.81707229594993E-17));
#9571=CARTESIAN_POINT('Origin',(0.,0.29,0.));
#9572=CARTESIAN_POINT('',(-0.5,0.0299999999999998,-6.12323399573677E-17));
#9573=CARTESIAN_POINT('Origin',(0.,0.0299999999999998,0.));
#9574=CARTESIAN_POINT('',(-0.5,0.29,-6.12323399573677E-17));
#9575=CARTESIAN_POINT('Origin',(0.,0.0150000000000001,0.));
#9576=CARTESIAN_POINT('',(-0.47,7.11236625150491E-17,-5.75583995599256E-17));
#9577=CARTESIAN_POINT('Origin',(0.,0.,0.));
#9578=CARTESIAN_POINT('',(-0.485,0.0150000000000001,-5.93953697586466E-17));
#9579=CARTESIAN_POINT('Origin',(0.32,0.,0.));
#9580=CARTESIAN_POINT('',(-0.32,-6.93889390390723E-18,-3.91886975727153E-17));
#9581=CARTESIAN_POINT('Origin',(0.,0.,0.));
#9582=CARTESIAN_POINT('Origin',(0.,-0.02,0.));
#9583=CARTESIAN_POINT('',(-0.2942,-0.0515999999999999,3.60291088309151E-17));
#9584=CARTESIAN_POINT('Origin',(0.,-0.0515999999999999,0.));
#9585=CARTESIAN_POINT('',(-0.31,-0.02,-3.7964050773568E-17));
#9586=CARTESIAN_POINT('Origin',(0.,-1.24,0.));
#9587=CARTESIAN_POINT('',(-0.2942,-2.4458,3.60291088309151E-17));
#9588=CARTESIAN_POINT('Origin',(0.,-2.4458,0.));
#9589=CARTESIAN_POINT('',(-0.2942,-1.24,-3.60291088309151E-17));
#9590=CARTESIAN_POINT('Origin',(0.,-2.47,0.));
#9591=CARTESIAN_POINT('',(-0.24,-2.5,-2.93915231795365E-17));
#9592=CARTESIAN_POINT('Origin',(0.,-2.5,0.));
#9593=CARTESIAN_POINT('',(-0.27,-2.47,-3.30654635769785E-17));
#9594=CARTESIAN_POINT('Origin',(0.,-2.5,0.));
#9595=CARTESIAN_POINT('Origin',(0.144337567297406,-0.6,-0.25));
#9596=CARTESIAN_POINT('',(0.288675134594813,-0.6,0.));
#9597=CARTESIAN_POINT('',(0.144337567297406,-0.6,-0.25));
#9598=CARTESIAN_POINT('',(0.288675134594813,-0.6,0.));
#9599=CARTESIAN_POINT('',(0.144337567297406,-0.96,-0.25));
#9600=CARTESIAN_POINT('',(0.144337567297406,-0.6,-0.25));
#9601=CARTESIAN_POINT('',(0.288675134594813,-0.96,0.));
#9602=CARTESIAN_POINT('',(0.288675134594813,-0.96,0.));
#9603=CARTESIAN_POINT('',(0.288675134594813,-0.6,0.));
#9604=CARTESIAN_POINT('Origin',(-0.144337567297406,-0.6,-0.25));
#9605=CARTESIAN_POINT('',(-0.144337567297406,-0.6,-0.25));
#9606=CARTESIAN_POINT('',(0.144337567297406,-0.6,-0.25));
#9607=CARTESIAN_POINT('',(-0.144337567297406,-0.96,-0.25));
#9608=CARTESIAN_POINT('',(-0.144337567297406,-0.6,-0.25));
#9609=CARTESIAN_POINT('',(0.144337567297406,-0.96,-0.25));
#9610=CARTESIAN_POINT('Origin',(-0.288675134594813,-0.6,-8.32667268468867E-17));
#9611=CARTESIAN_POINT('',(-0.288675134594813,-0.6,-3.53525079574969E-17));
#9612=CARTESIAN_POINT('',(-0.144337567297406,-0.6,-0.25));
#9613=CARTESIAN_POINT('',(-0.288675134594813,-0.96,-5.55111512312578E-17));
#9614=CARTESIAN_POINT('',(-0.288675134594813,-0.6,-3.53525079574969E-17));
#9615=CARTESIAN_POINT('',(-0.144337567297406,-0.96,-0.25));
#9616=CARTESIAN_POINT('Origin',(-0.144337567297407,-0.6,0.25));
#9617=CARTESIAN_POINT('',(-0.144337567297407,-0.6,0.25));
#9618=CARTESIAN_POINT('',(-0.288675134594813,-0.6,-3.53525079574969E-17));
#9619=CARTESIAN_POINT('',(-0.144337567297407,-0.96,0.25));
#9620=CARTESIAN_POINT('',(-0.144337567297407,-0.6,0.25));
#9621=CARTESIAN_POINT('',(-0.288675134594813,-0.96,-3.53525079574969E-17));
#9622=CARTESIAN_POINT('Origin',(0.144337567297406,-0.6,0.25));
#9623=CARTESIAN_POINT('',(0.144337567297406,-0.6,0.25));
#9624=CARTESIAN_POINT('',(-0.144337567297407,-0.6,0.25));
#9625=CARTESIAN_POINT('',(0.144337567297406,-0.96,0.25));
#9626=CARTESIAN_POINT('',(0.144337567297406,-0.6,0.25));
#9627=CARTESIAN_POINT('',(-0.144337567297407,-0.96,0.25));
#9628=CARTESIAN_POINT('Origin',(0.288675134594813,-0.6,0.));
#9629=CARTESIAN_POINT('',(0.144337567297406,-0.6,0.25));
#9630=CARTESIAN_POINT('',(0.144337567297406,-0.96,0.25));
#9631=CARTESIAN_POINT('Origin',(0.,-0.6,0.));
#9632=CARTESIAN_POINT('Origin',(0.,-0.96,0.));
#10926=UNCERTAINTY_MEASURE_WITH_UNIT(LENGTH_MEASURE(0.001),#10964,
'DISTANCE_ACCURACY_VALUE',
'Maximum model space distance between geometric entities at asserted c
onnectivities');
#10936=UNCERTAINTY_MEASURE_WITH_UNIT(LENGTH_MEASURE(0.001),#10964,
'DISTANCE_ACCURACY_VALUE',
'Maximum model space distance between geometric entities at asserted c
onnectivities');
#10953=(
GEOMETRIC_REPRESENTATION_CONTEXT(3)
GLOBAL_UNCERTAINTY_ASSIGNED_CONTEXT((#10926))
GLOBAL_UNIT_ASSIGNED_CONTEXT((#10964,#10966,#10967))
REPRESENTATION_CONTEXT('','3D')
);
#10963=(
GEOMETRIC_REPRESENTATION_CONTEXT(3)
GLOBAL_UNCERTAINTY_ASSIGNED_CONTEXT((#10936))
GLOBAL_UNIT_ASSIGNED_CONTEXT((#10964,#10966,#10967))
REPRESENTATION_CONTEXT('','3D')
);
#10964=(
LENGTH_UNIT()
NAMED_UNIT(*)
SI_UNIT(.CENTI.,.METRE.)
);
#10966=(
NAMED_UNIT(*)
PLANE_ANGLE_UNIT()
SI_UNIT($,.RADIAN.)
);
#10967=(
NAMED_UNIT(*)
SI_UNIT($,.STERADIAN.)
SOLID_ANGLE_UNIT()
);
#10984=SHAPE_DEFINITION_REPRESENTATION(#11015,#11073);
#11015=PRODUCT_DEFINITION_SHAPE('',$,#11100);
#11073=SHAPE_REPRESENTATION('',(#6245),#10953);
#11083=PRODUCT_DEFINITION_CONTEXT('part definition',#11163,'design');
#11100=PRODUCT_DEFINITION('Cap Screw - M6x25','Cap Screw - M6x25',#11126,
#11083);
#11126=PRODUCT_DEFINITION_FORMATION('',$,#11181);
#11163=APPLICATION_CONTEXT(
'Core Data for Automotive Mechanical Design Process');
#11164=PRODUCT_CONTEXT('part definition',#11163,'mechanical');
#11181=PRODUCT('Cap Screw - M6x25','Cap Screw - M6x25',
'Cap Screw - M6x25',(#11164));
#11254=COLOUR_RGB('Black',0.12,0.14,0.17);
#11255=FILL_AREA_STYLE_COLOUR('',#11254);
#11256=FILL_AREA_STYLE('',(#11255));
#11257=SURFACE_STYLE_FILL_AREA(#11256);
#11258=SURFACE_SIDE_STYLE('',(#11257));
#11259=SURFACE_STYLE_USAGE(.BOTH.,#11258);
#11260=PRESENTATION_STYLE_ASSIGNMENT((#11259));
ENDSEC;
END-ISO-10303-21;
